ISO-10303-21;
HEADER;
/* Generated by software containing ST-Developer
 * from STEP Tools, Inc. (www.steptools.com) 
 */

FILE_DESCRIPTION(
/* description */ ('Bin tilter linkage'),
/* implementation_level */ '2;1');

FILE_NAME(
/* name */ 'M4 short cap screw (25).step',
/* time_stamp */ '2026-10-28T03:26:24-07:00',
/* author */ (''),
/* organization */ (''),
/* preprocessor_version */ 'ST-DEVELOPER v20.2',
/* originating_system */ 'Autodesk Translation Framework v15.17.0.0',
/* authorisation */ '');

FILE_SCHEMA (('AUTOMOTIVE_DESIGN { 1 0 10303 214 3 1 1 }'));
ENDSEC;

DATA;
#10=MECHANICAL_DESIGN_GEOMETRIC_PRESENTATION_REPRESENTATION('',(#926),#23728);
#714=SHAPE_REPRESENTATION_RELATIONSHIP('SRR','None',#24180,#820);
#820=ADVANCED_BREP_SHAPE_REPRESENTATION('',(#1039),#23680);
#926=STYLED_ITEM('',(#24772),#1039);
#1039=MANIFOLD_SOLID_BREP('Body1',#12457);
#1369=FACE_BOUND('',#3412,.T.);
#1714=PLANE('',#14683);
#1715=PLANE('',#14688);
#1716=PLANE('',#14691);
#2352=FACE_OUTER_BOUND('',#3411,.T.);
#2353=FACE_OUTER_BOUND('',#3413,.T.);
#2354=FACE_OUTER_BOUND('',#3414,.T.);
#2355=FACE_OUTER_BOUND('',#3415,.T.);
#2356=FACE_OUTER_BOUND('',#3416,.T.);
#3411=EDGE_LOOP('',(#10093));
#3412=EDGE_LOOP('',(#10094));
#3413=EDGE_LOOP('',(#10095,#10096,#10097,#10098));
#3414=EDGE_LOOP('',(#10099));
#3415=EDGE_LOOP('',(#10100,#10101,#10102,#10103));
#3416=EDGE_LOOP('',(#10104));
#4233=LINE('',#21715,#4908);
#4234=LINE('',#21721,#4909);
#4908=VECTOR('',#17880,0.350000000000001);
#4909=VECTOR('',#17889,0.199999999999999);
#5675=CIRCLE('',#14684,0.350000000000001);
#5676=CIRCLE('',#14685,0.199999999999999);
#5677=CIRCLE('',#14687,0.350000000000001);
#5678=CIRCLE('',#14690,0.199999999999999);
#6529=VERTEX_POINT('',#21709);
#6530=VERTEX_POINT('',#21711);
#6531=VERTEX_POINT('',#21714);
#6532=VERTEX_POINT('',#21719);
#7786=EDGE_CURVE('',#6529,#6529,#5675,.T.);
#7787=EDGE_CURVE('',#6530,#6530,#5676,.T.);
#7788=EDGE_CURVE('',#6529,#6531,#4233,.T.);
#7789=EDGE_CURVE('',#6531,#6531,#5677,.T.);
#7790=EDGE_CURVE('',#6532,#6532,#5678,.T.);
#7791=EDGE_CURVE('',#6532,#6530,#4234,.T.);
#10093=ORIENTED_EDGE('',*,*,#7786,.T.);
#10094=ORIENTED_EDGE('',*,*,#7787,.F.);
#10095=ORIENTED_EDGE('',*,*,#7786,.F.);
#10096=ORIENTED_EDGE('',*,*,#7788,.T.);
#10097=ORIENTED_EDGE('',*,*,#7789,.T.);
#10098=ORIENTED_EDGE('',*,*,#7788,.F.);
#10099=ORIENTED_EDGE('',*,*,#7789,.F.);
#10100=ORIENTED_EDGE('',*,*,#7790,.F.);
#10101=ORIENTED_EDGE('',*,*,#7791,.T.);
#10102=ORIENTED_EDGE('',*,*,#7787,.T.);
#10103=ORIENTED_EDGE('',*,*,#7791,.F.);
#10104=ORIENTED_EDGE('',*,*,#7790,.T.);
#11503=CYLINDRICAL_SURFACE('',#14686,0.350000000000001);
#11504=CYLINDRICAL_SURFACE('',#14689,0.199999999999999);
#12077=ADVANCED_FACE('',(#2352,#1369),#1714,.T.);
#12078=ADVANCED_FACE('',(#2353),#11503,.T.);
#12079=ADVANCED_FACE('',(#2354),#1715,.F.);
#12080=ADVANCED_FACE('',(#2355),#11504,.T.);
#12081=ADVANCED_FACE('',(#2356),#1716,.T.);
#12457=CLOSED_SHELL('',(#12077,#12078,#12079,#12080,#12081));
#14682=AXIS2_PLACEMENT_3D('',#21707,#17870,#17871);
#14683=AXIS2_PLACEMENT_3D('',#21708,#17872,#17873);
#14684=AXIS2_PLACEMENT_3D('',#21710,#17874,#17875);
#14685=AXIS2_PLACEMENT_3D('',#21712,#17876,#17877);
#14686=AXIS2_PLACEMENT_3D('',#21713,#17878,#17879);
#14687=AXIS2_PLACEMENT_3D('',#21716,#17881,#17882);
#14688=AXIS2_PLACEMENT_3D('',#21717,#17883,#17884);
#14689=AXIS2_PLACEMENT_3D('',#21718,#17885,#17886);
#14690=AXIS2_PLACEMENT_3D('',#21720,#17887,#17888);
#14691=AXIS2_PLACEMENT_3D('',#21722,#17890,#17891);
#17870=DIRECTION('axis',(0.,0.,1.));
#17871=DIRECTION('refdir',(1.,0.,0.));
#17872=DIRECTION('center_axis',(0.,1.,0.));
#17873=DIRECTION('ref_axis',(1.,0.,0.));
#17874=DIRECTION('center_axis',(0.,1.,0.));
#17875=DIRECTION('ref_axis',(1.,0.,0.));
#17876=DIRECTION('center_axis',(0.,1.,0.));
#17877=DIRECTION('ref_axis',(1.,0.,0.));
#17878=DIRECTION('center_axis',(0.,1.,0.));
#17879=DIRECTION('ref_axis',(1.,0.,0.));
#17880=DIRECTION('',(0.,-1.,0.));
#17881=DIRECTION('center_axis',(0.,1.,0.));
#17882=DIRECTION('ref_axis',(1.,0.,0.));
#17883=DIRECTION('center_axis',(0.,1.,0.));
#17884=DIRECTION('ref_axis',(1.,0.,0.));
#17885=DIRECTION('center_axis',(0.,1.,0.));
#17886=DIRECTION('ref_axis',(1.,0.,0.));
#17887=DIRECTION('center_axis',(0.,1.,0.));
#17888=DIRECTION('ref_axis',(1.,0.,0.));
#17889=DIRECTION('',(0.,-1.,0.));
#17890=DIRECTION('center_axis',(0.,1.,0.));
#17891=DIRECTION('ref_axis',(1.,0.,0.));
#21707=CARTESIAN_POINT('',(0.,0.,0.));
#21708=CARTESIAN_POINT('Origin',(22.893930933827,-0.8,29.9659007476824));
#21709=CARTESIAN_POINT('',(22.543930933827,-0.8,29.9659007476824));
#21710=CARTESIAN_POINT('Origin',(22.893930933827,-0.8,29.9659007476824));
#21711=CARTESIAN_POINT('',(22.693930933827,-0.8,29.9659007476824));
#21712=CARTESIAN_POINT('Origin',(22.893930933827,-0.8,29.9659007476824));
#21713=CARTESIAN_POINT('Origin',(22.893930933827,-1.2,29.9659007476824));
#21714=CARTESIAN_POINT('',(22.543930933827,-1.2,29.9659007476824));
#21715=CARTESIAN_POINT('',(22.543930933827,-1.2,29.9659007476824));
#21716=CARTESIAN_POINT('Origin',(22.893930933827,-1.2,29.9659007476824));
#21717=CARTESIAN_POINT('Origin',(22.893930933827,-1.2,29.9659007476824));
#21718=CARTESIAN_POINT('Origin',(22.893930933827,-0.8,29.9659007476824));
#21719=CARTESIAN_POINT('',(22.693930933827,-0.1,29.9659007476824));
#21720=CARTESIAN_POINT('Origin',(22.893930933827,-0.1,29.9659007476824));
#21721=CARTESIAN_POINT('',(22.693930933827,-0.8,29.9659007476824));
#21722=CARTESIAN_POINT('Origin',(22.893930933827,-0.1,29.9659007476824));
#23563=UNCERTAINTY_MEASURE_WITH_UNIT(LENGTH_MEASURE(0.001),#23729,
'DISTANCE_ACCURACY_VALUE',
'Maximum model space distance between geometric entities at asserted c
onnectivities');
#23611=UNCERTAINTY_MEASURE_WITH_UNIT(LENGTH_MEASURE(0.001),#23729,
'DISTANCE_ACCURACY_VALUE',
'Maximum model space distance between geometric entities at asserted c
onnectivities');
#23680=(
GEOMETRIC_REPRESENTATION_CONTEXT(3)
GLOBAL_UNCERTAINTY_ASSIGNED_CONTEXT((#23563))
GLOBAL_UNIT_ASSIGNED_CONTEXT((#23729,#23731,#23732))
REPRESENTATION_CONTEXT('','3D')
);
#23728=(
GEOMETRIC_REPRESENTATION_CONTEXT(3)
GLOBAL_UNCERTAINTY_ASSIGNED_CONTEXT((#23611))
GLOBAL_UNIT_ASSIGNED_CONTEXT((#23729,#23731,#23732))
REPRESENTATION_CONTEXT('','3D')
);
#23729=(
LENGTH_UNIT()
NAMED_UNIT(*)
SI_UNIT(.CENTI.,.METRE.)
);
#23731=(
NAMED_UNIT(*)
PLANE_ANGLE_UNIT()
SI_UNIT($,.RADIAN.)
);
#23732=(
NAMED_UNIT(*)
SI_UNIT($,.STERADIAN.)
SOLID_ANGLE_UNIT()
);
#23801=SHAPE_DEFINITION_REPRESENTATION(#23917,#24180);
#23917=PRODUCT_DEFINITION_SHAPE('',$,#24297);
#24180=SHAPE_REPRESENTATION('',(#14682),#23680);
#24228=PRODUCT_DEFINITION_CONTEXT('part definition',#24578,'design');
#24297=PRODUCT_DEFINITION('M4 short cap screw (25)',
'M4 short cap screw (25)',#24413,#24228);
#24413=PRODUCT_DEFINITION_FORMATION('',$,#24648);
#24578=APPLICATION_CONTEXT(
'Core Data for Automotive Mechanical Design Process');
#24579=PRODUCT_CONTEXT('part definition',#24578,'mechanical');
#24648=PRODUCT('M4 short cap screw (25)','M4 short cap screw (25)',
'M4 short cap screw (25)',(#24579));
#24766=COLOUR_RGB('Black',0.12,0.14,0.17);
#24767=FILL_AREA_STYLE_COLOUR('',#24766);
#24768=FILL_AREA_STYLE('',(#24767));
#24769=SURFACE_STYLE_FILL_AREA(#24768);
#24770=SURFACE_SIDE_STYLE('',(#24769));
#24771=SURFACE_STYLE_USAGE(.BOTH.,#24770);
#24772=PRESENTATION_STYLE_ASSIGNMENT((#24771));
ENDSEC;
END-ISO-10303-21;
